ISO-10303-21;
HEADER;
/* Generated by software containing ST-Developer
 * from STEP Tools, Inc. (www.steptools.com) 
 */

FILE_DESCRIPTION(
/* description */ ('Turntable on roller ring'),
/* implementation_level */ '2;1');

FILE_NAME(
/* name */ 'Axle keeper (1).step',
/* time_stamp */ '2026-10-28T03:23:59-07:00',
/* author */ (''),
/* organization */ (''),
/* preprocessor_version */ 'ST-DEVELOPER v20.2',
/* originating_system */ 'Autodesk Translation Framework v15.17.0.0',
/* authorisation */ '');

FILE_SCHEMA (('AUTOMOTIVE_DESIGN { 1 0 10303 214 3 1 1 }'));
ENDSEC;

DATA;
#10=MECHANICAL_DESIGN_GEOMETRIC_PRESENTATION_REPRESENTATION('',(#651),#16281);
#532=SHAPE_REPRESENTATION_RELATIONSHIP('SRR','None',#16550,#587);
#587=ADVANCED_BREP_SHAPE_REPRESENTATION('',(#721),#16244);
#651=STYLED_ITEM('',(#16932),#721);
#721=MANIFOLD_SOLID_BREP('Body1',#8394);
#909=FACE_BOUND('',#2198,.T.);
#910=FACE_BOUND('',#2200,.T.);
#1133=PLANE('',#9684);
#1134=PLANE('',#9685);
#1538=FACE_OUTER_BOUND('',#2195,.T.);
#1539=FACE_OUTER_BOUND('',#2196,.T.);
#1540=FACE_OUTER_BOUND('',#2197,.T.);
#1541=FACE_OUTER_BOUND('',#2199,.T.);
#2195=EDGE_LOOP('',(#6857,#6858,#6859,#6860));
#2196=EDGE_LOOP('',(#6861,#6862,#6863,#6864));
#2197=EDGE_LOOP('',(#6865));
#2198=EDGE_LOOP('',(#6866));
#2199=EDGE_LOOP('',(#6867));
#2200=EDGE_LOOP('',(#6868));
#2786=LINE('',#14802,#3269);
#2787=LINE('',#14808,#3270);
#3269=VECTOR('',#11773,0.225);
#3270=VECTOR('',#11780,0.8);
#3751=CIRCLE('',#9679,0.225);
#3752=CIRCLE('',#9680,0.225);
#3753=CIRCLE('',#9682,0.8);
#3754=CIRCLE('',#9683,0.8);
#4355=VERTEX_POINT('',#14799);
#4356=VERTEX_POINT('',#14801);
#4357=VERTEX_POINT('',#14805);
#4358=VERTEX_POINT('',#14807);
#5239=EDGE_CURVE('',#4355,#4355,#3751,.T.);
#5240=EDGE_CURVE('',#4355,#4356,#2786,.T.);
#5241=EDGE_CURVE('',#4356,#4356,#3752,.T.);
#5242=EDGE_CURVE('',#4357,#4357,#3753,.T.);
#5243=EDGE_CURVE('',#4357,#4358,#2787,.T.);
#5244=EDGE_CURVE('',#4358,#4358,#3754,.T.);
#6857=ORIENTED_EDGE('',*,*,#5239,.F.);
#6858=ORIENTED_EDGE('',*,*,#5240,.T.);
#6859=ORIENTED_EDGE('',*,*,#5241,.T.);
#6860=ORIENTED_EDGE('',*,*,#5240,.F.);
#6861=ORIENTED_EDGE('',*,*,#5242,.F.);
#6862=ORIENTED_EDGE('',*,*,#5243,.T.);
#6863=ORIENTED_EDGE('',*,*,#5244,.T.);
#6864=ORIENTED_EDGE('',*,*,#5243,.F.);
#6865=ORIENTED_EDGE('',*,*,#5242,.T.);
#6866=ORIENTED_EDGE('',*,*,#5239,.T.);
#6867=ORIENTED_EDGE('',*,*,#5244,.F.);
#6868=ORIENTED_EDGE('',*,*,#5241,.F.);
#7781=CYLINDRICAL_SURFACE('',#9678,0.225);
#7782=CYLINDRICAL_SURFACE('',#9681,0.8);
#8141=ADVANCED_FACE('',(#1538),#7781,.F.);
#8142=ADVANCED_FACE('',(#1539),#7782,.T.);
#8143=ADVANCED_FACE('',(#1540,#909),#1133,.T.);
#8144=ADVANCED_FACE('',(#1541,#910),#1134,.F.);
#8394=CLOSED_SHELL('',(#8141,#8142,#8143,#8144));
#9677=AXIS2_PLACEMENT_3D('',#14797,#11767,#11768);
#9678=AXIS2_PLACEMENT_3D('',#14798,#11769,#11770);
#9679=AXIS2_PLACEMENT_3D('',#14800,#11771,#11772);
#9680=AXIS2_PLACEMENT_3D('',#14803,#11774,#11775);
#9681=AXIS2_PLACEMENT_3D('',#14804,#11776,#11777);
#9682=AXIS2_PLACEMENT_3D('',#14806,#11778,#11779);
#9683=AXIS2_PLACEMENT_3D('',#14809,#11781,#11782);
#9684=AXIS2_PLACEMENT_3D('',#14810,#11783,#11784);
#9685=AXIS2_PLACEMENT_3D('',#14811,#11785,#11786);
#11767=DIRECTION('axis',(0.,0.,1.));
#11768=DIRECTION('refdir',(1.,0.,0.));
#11769=DIRECTION('center_axis',(0.,1.,0.));
#11770=DIRECTION('ref_axis',(1.,0.,0.));
#11771=DIRECTION('center_axis',(0.,-1.,0.));
#11772=DIRECTION('ref_axis',(1.,0.,0.));
#11773=DIRECTION('',(0.,-1.,0.));
#11774=DIRECTION('center_axis',(0.,-1.,0.));
#11775=DIRECTION('ref_axis',(1.,0.,0.));
#11776=DIRECTION('center_axis',(0.,1.,0.));
#11777=DIRECTION('ref_axis',(1.,0.,0.));
#11778=DIRECTION('center_axis',(0.,1.,0.));
#11779=DIRECTION('ref_axis',(1.,0.,0.));
#11780=DIRECTION('',(0.,-1.,0.));
#11781=DIRECTION('center_axis',(0.,1.,0.));
#11782=DIRECTION('ref_axis',(1.,0.,0.));
#11783=DIRECTION('center_axis',(0.,1.,0.));
#11784=DIRECTION('ref_axis',(1.,0.,0.));
#11785=DIRECTION('center_axis',(0.,1.,0.));
#11786=DIRECTION('ref_axis',(1.,0.,0.));
#14797=CARTESIAN_POINT('',(0.,0.,0.));
#14798=CARTESIAN_POINT('Origin',(0.,16.3,3.5));
#14799=CARTESIAN_POINT('',(-0.225,16.5,3.5));
#14800=CARTESIAN_POINT('Origin',(0.,16.5,3.5));
#14801=CARTESIAN_POINT('',(-0.225,16.3,3.5));
#14802=CARTESIAN_POINT('',(-0.225,16.3,3.5));
#14803=CARTESIAN_POINT('Origin',(0.,16.3,3.5));
#14804=CARTESIAN_POINT('Origin',(0.,16.3,3.5));
#14805=CARTESIAN_POINT('',(-0.8,16.5,3.5));
#14806=CARTESIAN_POINT('Origin',(0.,16.5,3.5));
#14807=CARTESIAN_POINT('',(-0.8,16.3,3.5));
#14808=CARTESIAN_POINT('',(-0.8,16.3,3.5));
#14809=CARTESIAN_POINT('Origin',(0.,16.3,3.5));
#14810=CARTESIAN_POINT('Origin',(0.,16.5,3.5));
#14811=CARTESIAN_POINT('Origin',(0.,16.3,3.5));
#16175=UNCERTAINTY_MEASURE_WITH_UNIT(LENGTH_MEASURE(0.001),#16282,
'DISTANCE_ACCURACY_VALUE',
'Maximum model space distance between geometric entities at asserted c
onnectivities');
#16212=UNCERTAINTY_MEASURE_WITH_UNIT(LENGTH_MEASURE(0.001),#16282,
'DISTANCE_ACCURACY_VALUE',
'Maximum model space distance between geometric entities at asserted c
onnectivities');
#16244=(
GEOMETRIC_REPRESENTATION_CONTEXT(3)
GLOBAL_UNCERTAINTY_ASSIGNED_CONTEXT((#16175))
GLOBAL_UNIT_ASSIGNED_CONTEXT((#16282,#16284,#16285))
REPRESENTATION_CONTEXT('','3D')
);
#16281=(
GEOMETRIC_REPRESENTATION_CONTEXT(3)
GLOBAL_UNCERTAINTY_ASSIGNED_CONTEXT((#16212))
GLOBAL_UNIT_ASSIGNED_CONTEXT((#16282,#16284,#16285))
REPRESENTATION_CONTEXT('','3D')
);
#16282=(
LENGTH_UNIT()
NAMED_UNIT(*)
SI_UNIT(.CENTI.,.METRE.)
);
#16284=(
NAMED_UNIT(*)
PLANE_ANGLE_UNIT()
SI_UNIT($,.RADIAN.)
);
#16285=(
NAMED_UNIT(*)
SI_UNIT($,.STERADIAN.)
SOLID_ANGLE_UNIT()
);
#16317=SHAPE_DEFINITION_REPRESENTATION(#16411,#16550);
#16411=PRODUCT_DEFINITION_SHAPE('',$,#16619);
#16550=SHAPE_REPRESENTATION('',(#9677),#16244);
#16587=PRODUCT_DEFINITION_CONTEXT('part definition',#16793,'design');
#16619=PRODUCT_DEFINITION('Axle keeper (1)','Axle keeper (1)',#16687,#16587);
#16687=PRODUCT_DEFINITION_FORMATION('',$,#16826);
#16793=APPLICATION_CONTEXT(
'Core Data for Automotive Mechanical Design Process');
#16794=PRODUCT_CONTEXT('part definition',#16793,'mechanical');
#16826=PRODUCT('Axle keeper (1)','Axle keeper (1)','Axle keeper (1)',(#16794));
#16926=COLOUR_RGB('Grey',0.48,0.52,0.57);
#16927=FILL_AREA_STYLE_COLOUR('',#16926);
#16928=FILL_AREA_STYLE('',(#16927));
#16929=SURFACE_STYLE_FILL_AREA(#16928);
#16930=SURFACE_SIDE_STYLE('',(#16929));
#16931=SURFACE_STYLE_USAGE(.BOTH.,#16930);
#16932=PRESENTATION_STYLE_ASSIGNMENT((#16931));
ENDSEC;
END-ISO-10303-21;
